ISO-10303-21;
HEADER;
/* Generated by software containing ST-Developer
 * from STEP Tools, Inc. (www.steptools.com) 
 */

FILE_DESCRIPTION(
/* description */ (''),
/* implementation_level */ '2;1');

FILE_NAME(
/* name */ 'Rod_02.step',
/* time_stamp */ '2026-10-05T15:35:09-07:00',
/* author */ (''),
/* organization */ (''),
/* preprocessor_version */ 'ST-DEVELOPER v20.2',
/* originating_system */ 'Autodesk Translation Framework v15.15.0.0',
/* authorisation */ '');

FILE_SCHEMA (('AUTOMOTIVE_DESIGN { 1 0 10303 214 3 1 1 }'));
ENDSEC;

DATA;
#10=MECHANICAL_DESIGN_GEOMETRIC_PRESENTATION_REPRESENTATION('',(#545),#74523);
#527=SHAPE_REPRESENTATION_RELATIONSHIP('SRR','None',#74560,#536);
#536=ADVANCED_BREP_SHAPE_REPRESENTATION('',(#554),#74516);
#545=STYLED_ITEM('',(#74612),#554);
#554=MANIFOLD_SOLID_BREP('Body1',#4724);
#635=PLANE('',#4930);
#636=PLANE('',#4934);
#731=FACE_OUTER_BOUND('',#895,.T.);
#732=FACE_OUTER_BOUND('',#896,.T.);
#733=FACE_OUTER_BOUND('',#897,.T.);
#895=EDGE_LOOP('',(#3216));
#896=EDGE_LOOP('',(#3217,#3218,#3219,#3220));
#897=EDGE_LOOP('',(#3221));
#1101=LINE('',#6103,#1298);
#1298=VECTOR('',#5387,6.00000000000001);
#1458=CIRCLE('',#4931,6.00000000000001);
#1459=CIRCLE('',#4933,6.00000000000001);
#1608=VERTEX_POINT('',#6098);
#1609=VERTEX_POINT('',#6101);
#2309=EDGE_CURVE('',#1608,#1608,#1458,.T.);
#2310=EDGE_CURVE('',#1609,#1609,#1459,.T.);
#2311=EDGE_CURVE('',#1609,#1608,#1101,.T.);
#3216=ORIENTED_EDGE('',*,*,#2309,.T.);
#3217=ORIENTED_EDGE('',*,*,#2310,.F.);
#3218=ORIENTED_EDGE('',*,*,#2311,.T.);
#3219=ORIENTED_EDGE('',*,*,#2309,.F.);
#3220=ORIENTED_EDGE('',*,*,#2311,.F.);
#3221=ORIENTED_EDGE('',*,*,#2310,.T.);
#4537=CYLINDRICAL_SURFACE('',#4932,6.00000000000001);
#4627=ADVANCED_FACE('',(#731),#635,.T.);
#4628=ADVANCED_FACE('',(#732),#4537,.T.);
#4629=ADVANCED_FACE('',(#733),#636,.F.);
#4724=CLOSED_SHELL('',(#4627,#4628,#4629));
#4929=AXIS2_PLACEMENT_3D('',#6096,#5377,#5378);
#4930=AXIS2_PLACEMENT_3D('',#6097,#5379,#5380);
#4931=AXIS2_PLACEMENT_3D('',#6099,#5381,#5382);
#4932=AXIS2_PLACEMENT_3D('',#6100,#5383,#5384);
#4933=AXIS2_PLACEMENT_3D('',#6102,#5385,#5386);
#4934=AXIS2_PLACEMENT_3D('',#6104,#5388,#5389);
#5377=DIRECTION('axis',(0.,0.,1.));
#5378=DIRECTION('refdir',(1.,0.,0.));
#5379=DIRECTION('center_axis',(0.,-1.,0.));
#5380=DIRECTION('ref_axis',(1.,0.,0.));
#5381=DIRECTION('center_axis',(0.,-1.,0.));
#5382=DIRECTION('ref_axis',(1.,0.,0.));
#5383=DIRECTION('center_axis',(0.,1.,0.));
#5384=DIRECTION('ref_axis',(1.,0.,0.));
#5385=DIRECTION('center_axis',(0.,1.,0.));
#5386=DIRECTION('ref_axis',(1.,0.,0.));
#5387=DIRECTION('',(0.,-1.,0.));
#5388=DIRECTION('center_axis',(0.,-1.,0.));
#5389=DIRECTION('ref_axis',(1.,0.,0.));
#6096=CARTESIAN_POINT('',(0.,0.,0.));
#6097=CARTESIAN_POINT('Origin',(60.231676812499,-95.,175.));
#6098=CARTESIAN_POINT('',(54.231676812499,-95.,175.));
#6099=CARTESIAN_POINT('Origin',(60.231676812499,-95.,175.));
#6100=CARTESIAN_POINT('Origin',(60.231676812499,-90.,175.));
#6101=CARTESIAN_POINT('',(54.231676812499,95.,175.));
#6102=CARTESIAN_POINT('Origin',(60.231676812499,95.,175.));
#6103=CARTESIAN_POINT('',(54.231676812499,-90.,175.));
#6104=CARTESIAN_POINT('Origin',(60.231676812499,95.,175.));
#74505=UNCERTAINTY_MEASURE_WITH_UNIT(LENGTH_MEASURE(0.01),#74524,
'DISTANCE_ACCURACY_VALUE',
'Maximum model space distance between geometric entities at asserted c
onnectivities');
#74512=UNCERTAINTY_MEASURE_WITH_UNIT(LENGTH_MEASURE(0.01),#74524,
'DISTANCE_ACCURACY_VALUE',
'Maximum model space distance between geometric entities at asserted c
onnectivities');
#74516=(
GEOMETRIC_REPRESENTATION_CONTEXT(3)
GLOBAL_UNCERTAINTY_ASSIGNED_CONTEXT((#74505))
GLOBAL_UNIT_ASSIGNED_CONTEXT((#74524,#74526,#74527))
REPRESENTATION_CONTEXT('','3D')
);
#74523=(
GEOMETRIC_REPRESENTATION_CONTEXT(3)
GLOBAL_UNCERTAINTY_ASSIGNED_CONTEXT((#74512))
GLOBAL_UNIT_ASSIGNED_CONTEXT((#74524,#74526,#74527))
REPRESENTATION_CONTEXT('','3D')
);
#74524=(
LENGTH_UNIT()
NAMED_UNIT(*)
SI_UNIT(.MILLI.,.METRE.)
);
#74526=(
NAMED_UNIT(*)
PLANE_ANGLE_UNIT()
SI_UNIT($,.RADIAN.)
);
#74527=(
NAMED_UNIT(*)
SI_UNIT($,.STERADIAN.)
SOLID_ANGLE_UNIT()
);
#74531=SHAPE_DEFINITION_REPRESENTATION(#74541,#74560);
#74541=PRODUCT_DEFINITION_SHAPE('',$,#74571);
#74560=SHAPE_REPRESENTATION('',(#4929),#74516);
#74567=PRODUCT_DEFINITION_CONTEXT('part definition',#74599,'design');
#74571=PRODUCT_DEFINITION('Rod_02','Rod_02',#74581,#74567);
#74581=PRODUCT_DEFINITION_FORMATION('',$,#74604);
#74599=APPLICATION_CONTEXT(
'Core Data for Automotive Mechanical Design Process');
#74600=PRODUCT_CONTEXT('part definition',#74599,'mechanical');
#74604=PRODUCT('Rod_02','Rod_02',$,(#74600));
#74612=PRESENTATION_STYLE_ASSIGNMENT((#74615));
#74615=SURFACE_STYLE_USAGE(.BOTH.,#74618);
#74618=SURFACE_SIDE_STYLE('',(#74621));
#74621=SURFACE_STYLE_FILL_AREA(#74624);
#74624=FILL_AREA_STYLE('Opaque(215,0,0)',(#74627));
#74627=FILL_AREA_STYLE_COLOUR('Opaque(215,0,0)',#74630);
#74630=COLOUR_RGB('Opaque(215,0,0)', 0.09019608, 0.27058824, 0.51372549);
ENDSEC;
END-ISO-10303-21;
